ISO-10303-21;
HEADER;
FILE_DESCRIPTION (('STEP AP203'),
    '1' );
FILE_NAME ('Cleco, Fastener, Pincher.step',
    '2026-10-09T13:45:32',
    ( '' ),
    ( '' ),
    'SwSTEP 2.0',
    'SolidWorks 2024',
    '' );
FILE_SCHEMA (( 'AUTOMOTIVE_DESIGN' ));
ENDSEC;

DATA;
#7=LINE ( 'NONE', #8071, #3494 ) ;
#14=CARTESIAN_POINT ( 'NONE',  ( 0.6250000000000000000, -0.07812500000000001388, 0.000000000000000000 ) ) ;
#48=CIRCLE ( 'NONE', #181, 0.3547681700190749576 ) ;
#80=EDGE_CURVE ( 'NONE', #1875, #4512, #6627, .T. ) ;
#104=DIRECTION ( 'NONE',  ( 1.821231995776175479E-16, 1.000000000000000000, 0.000000000000000000 ) ) ;
#135=DIRECTION ( 'NONE',  ( 1.000000000000000000, 0.000000000000000000, 0.000000000000000000 ) ) ;
#147=CARTESIAN_POINT ( 'NONE',  ( 0.2896281645421511231, -0.04777128394798136474, 0.07449999999999999678 ) ) ;
#167=LINE ( 'NONE', #5090, #7384 ) ;
#181=AXIS2_PLACEMENT_3D ( 'NONE', #5513, #3140, #511 ) ;
#226=ADVANCED_FACE ( 'NONE', ( #1827 ), #5682, .F. ) ;
#249=CARTESIAN_POINT ( 'NONE',  ( 0.2896281645421511231, -0.04777128394798136474, 0.07449999999999999678 ) ) ;
#256=ORIENTED_EDGE ( 'NONE', *, *, #330, .T. ) ;
#270=EDGE_CURVE ( 'NONE', #5976, #1875, #3258, .T. ) ;
#281=DIRECTION ( 'NONE',  ( -0.000000000000000000, -0.000000000000000000, -1.000000000000000000 ) ) ;
#304=EDGE_LOOP ( 'NONE', ( #7542, #4529, #3682, #1925 ) ) ;
#330=EDGE_CURVE ( 'NONE', #6252, #7690, #7566, .T. ) ;
#331=DIRECTION ( 'NONE',  ( 0.000000000000000000, -0.000000000000000000, -1.000000000000000000 ) ) ;
#381=CARTESIAN_POINT ( 'NONE',  ( -0.04782642554762442377, -0.07812500000000000000, 0.07449999999999999678 ) ) ;
#432=DIRECTION ( 'NONE',  ( -0.000000000000000000, -0.000000000000000000, -1.000000000000000000 ) ) ;
#452=EDGE_LOOP ( 'NONE', ( #3653, #4047, #3195, #3348, #4965, #4902, #4700, #4010 ) ) ;
#459=ORIENTED_EDGE ( 'NONE', *, *, #5093, .F. ) ;
#504=( NAMED_UNIT ( * ) PLANE_ANGLE_UNIT ( ) SI_UNIT ( $, .RADIAN. ) );
#511=DIRECTION ( 'NONE',  ( -1.000000000000000000, 0.000000000000000000, 0.000000000000000000 ) ) ;
#534=CARTESIAN_POINT ( 'NONE',  ( 0.2896281645421511231, -0.04777128394798136474, 0.07449999999999999678 ) ) ;
#553=( GEOMETRIC_REPRESENTATION_CONTEXT ( 3 ) GLOBAL_UNCERTAINTY_ASSIGNED_CONTEXT ( ( #1860 ) ) GLOBAL_UNIT_ASSIGNED_CONTEXT ( ( #3627, #504, #3086 ) ) REPRESENTATION_CONTEXT ( 'NONE', 'WORKASPACE' ) );
#582=AXIS2_PLACEMENT_3D ( 'NONE', #2056, #3937, #331 ) ;
#599=FACE_OUTER_BOUND ( 'NONE', #452, .T. ) ;
#608=EDGE_LOOP ( 'NONE', ( #844, #5618, #7567, #2480 ) ) ;
#663=DIRECTION ( 'NONE',  ( -1.821231995776175725E-16, -1.000000000000000000, 0.000000000000000000 ) ) ;
#708=DIRECTION ( 'NONE',  ( -1.000000000000000000, 0.000000000000000000, 0.000000000000000000 ) ) ;
#711=AXIS2_PLACEMENT_3D ( 'NONE', #6403, #5171, #708 ) ;
#731=VECTOR ( 'NONE', #2411, 39.37007874015748143 ) ;
#733=ORIENTED_EDGE ( 'NONE', *, *, #3536, .T. ) ;
#777=VERTEX_POINT ( 'NONE', #824 ) ;
#824=CARTESIAN_POINT ( 'NONE',  ( 0.6597999294535048520, -0.04777128394798136474, 0.07449999999999999678 ) ) ;
#827=ADVANCED_FACE ( 'NONE', ( #7752 ), #2098, .F. ) ;
#841=ORIENTED_EDGE ( 'NONE', *, *, #3148, .T. ) ;
#844=ORIENTED_EDGE ( 'NONE', *, *, #3027, .T. ) ;
#900=ADVANCED_FACE ( 'NONE', ( #5461 ), #7949, .F. ) ;
#910=CARTESIAN_POINT ( 'NONE',  ( 0.6645694204159616758, 0.008319420416198241783, 0.000000000000000000 ) ) ;
#922=ORIENTED_EDGE ( 'NONE', *, *, #5339, .T. ) ;
#959=ORIENTED_EDGE ( 'NONE', *, *, #6499, .T. ) ;
#994=EDGE_CURVE ( 'NONE', #5472, #5976, #1155, .T. ) ;
#1002=ORIENTED_EDGE ( 'NONE', *, *, #5487, .T. ) ;
#1018=VERTEX_POINT ( 'NONE', #534 ) ;
#1031=CARTESIAN_POINT ( 'NONE',  ( 0.6597999294535048520, -0.01652128394798136821, 0.07449999999999999678 ) ) ;
#1041=ORIENTED_EDGE ( 'NONE', *, *, #4042, .T. ) ;
#1155=LINE ( 'NONE', #2957, #731 ) ;
#1200=VERTEX_POINT ( 'NONE', #1345 ) ;
#1301=LINE ( 'NONE', #1419, #3838 ) ;
#1312=CARTESIAN_POINT ( 'NONE',  ( 0.7510138408322231118, -0.03124999999962550443, 0.07449999999999999678 ) ) ;
#1345=CARTESIAN_POINT ( 'NONE',  ( 0.7510138408322231118, -0.03124999999962550443, 0.000000000000000000 ) ) ;
#1361=DIRECTION ( 'NONE',  ( -0.000000000000000000, -0.000000000000000000, -1.000000000000000000 ) ) ;
#1419=CARTESIAN_POINT ( 'NONE',  ( 0.2386870781737283065, -0.03125000000000000000, 0.000000000000000000 ) ) ;
#1433=DIRECTION ( 'NONE',  ( -1.000000000000000000, -0.000000000000000000, -0.000000000000000000 ) ) ;
#1447=ORIENTED_EDGE ( 'NONE', *, *, #5093, .T. ) ;
#1492=CARTESIAN_POINT ( 'NONE',  ( 0.6690408158126811555, -0.04637372973215107830, 0.07449999999999999678 ) ) ;
#1501=VERTEX_POINT ( 'NONE', #6111 ) ;
#1625=DIRECTION ( 'NONE',  ( 0.000000000000000000, 0.000000000000000000, 1.000000000000000000 ) ) ;
#1634=AXIS2_PLACEMENT_3D ( 'NONE', #6302, #3951, #104 ) ;
#1700=DIRECTION ( 'NONE',  ( -1.000000000000000000, 0.000000000000000000, 0.000000000000000000 ) ) ;
#1728=ORIENTED_EDGE ( 'NONE', *, *, #4183, .T. ) ;
#1769=DIRECTION ( 'NONE',  ( -0.000000000000000000, -0.000000000000000000, -1.000000000000000000 ) ) ;
#1791=VECTOR ( 'NONE', #5009, 39.37007874015748143 ) ;
#1811=DIRECTION ( 'NONE',  ( 0.000000000000000000, -0.000000000000000000, 1.000000000000000000 ) ) ;
#1822=DIRECTION ( 'NONE',  ( -0.000000000000000000, -0.000000000000000000, -1.000000000000000000 ) ) ;
#1827=FACE_OUTER_BOUND ( 'NONE', #3699, .T. ) ;
#1839=ORIENTED_EDGE ( 'NONE', *, *, #5487, .F. ) ;
#1841=CARTESIAN_POINT ( 'NONE',  ( 0.6597999294535048520, -0.04777128394798136474, 0.07449999999999999678 ) ) ;
#1860=UNCERTAINTY_MEASURE_WITH_UNIT (LENGTH_MEASURE( 1.000000000000000082E-05 ), #3627, 'distance_accuracy_value', 'NONE');
#1873=ADVANCED_FACE ( 'NONE', ( #599 ), #5753, .T. ) ;
#1875=VERTEX_POINT ( 'NONE', #6868 ) ;
#1925=ORIENTED_EDGE ( 'NONE', *, *, #6442, .T. ) ;
#1981=ADVANCED_BREP_SHAPE_REPRESENTATION ( '', ( #3593, #3555 ), #553 ) ;
#2020=CARTESIAN_POINT ( 'NONE',  ( 0.6597999294535048520, -0.01652128394798136821, 0.000000000000000000 ) ) ;
#2048=CARTESIAN_POINT ( 'NONE',  ( -0.04782642554762442377, -0.07812500000000000000, 0.000000000000000000 ) ) ;
#2056=CARTESIAN_POINT ( 'NONE',  ( 0.2896281645421511231, -0.04777128394798136474, 0.07449999999999999678 ) ) ;
#2071=ORIENTED_EDGE ( 'NONE', *, *, #6423, .T. ) ;
#2098=PLANE ( 'NONE',  #2176 ) ;
#2109=PRODUCT_DEFINITION_SHAPE ( 'NONE', 'NONE',  #6001 ) ;
#2137=FACE_OUTER_BOUND ( 'NONE', #2907, .T. ) ;
#2154=ORIENTED_EDGE ( 'NONE', *, *, #4545, .T. ) ;
#2176=AXIS2_PLACEMENT_3D ( 'NONE', #2258, #4597, #7185 ) ;
#2190=EDGE_CURVE ( 'NONE', #6170, #4512, #5585, .T. ) ;
#2252=CYLINDRICAL_SURFACE ( 'NONE', #5957, 0.03124999999999997571 ) ;
#2258=CARTESIAN_POINT ( 'NONE',  ( 0.2935750530104211387, 0.05119392622207447063, 0.07449999999999999678 ) ) ;
#2303=AXIS2_PLACEMENT_3D ( 'NONE', #7291, #281, #5905 ) ;
#2307=CARTESIAN_POINT ( 'NONE',  ( -0.04782642554762441683, -0.03125000000000000000, 0.07449999999999999678 ) ) ;
#2314=CYLINDRICAL_SURFACE ( 'NONE', #3372, 0.09507037842118626347 ) ;
#2315=AXIS2_PLACEMENT_3D ( 'NONE', #4228, #7720, #3950 ) ;
#2352=CYLINDRICAL_SURFACE ( 'NONE', #5196, 0.3547681700190749576 ) ;
#2411=DIRECTION ( 'NONE',  ( -1.821231995776175725E-16, -1.000000000000000000, 0.000000000000000000 ) ) ;
#2425=AXIS2_PLACEMENT_3D ( 'NONE', #6244, #7380, #1811 ) ;
#2480=ORIENTED_EDGE ( 'NONE', *, *, #2190, .T. ) ;
#2567=CARTESIAN_POINT ( 'NONE',  ( 0.7739487307887357170, -0.3852760516983189110, 0.000000000000000000 ) ) ;
#2590=FACE_OUTER_BOUND ( 'NONE', #304, .T. ) ;
#2636=ORIENTED_EDGE ( 'NONE', *, *, #3148, .F. ) ;
#2641=DIRECTION ( 'NONE',  ( -0.000000000000000000, -0.000000000000000000, -1.000000000000000000 ) ) ;
#2660=LINE ( 'NONE', #249, #3860 ) ;
#2683=VECTOR ( 'NONE', #3914, 39.37007874015748143 ) ;
#2713=VECTOR ( 'NONE', #2807, 39.37007874015748143 ) ;
#2732=CARTESIAN_POINT ( 'NONE',  ( -0.04782642554762441683, -0.03125000000000000000, 0.07449999999999999678 ) ) ;
#2735=DIRECTION ( 'NONE',  ( 1.000000000000000000, 0.000000000000000000, 0.000000000000000000 ) ) ;
#2765=DESIGN_CONTEXT ( 'detailed design', #3474, 'design' ) ;
#2780=EDGE_CURVE ( 'NONE', #3425, #6917, #1301, .T. ) ;
#2796=MECHANICAL_CONTEXT ( 'NONE', #4728, 'mechanical' ) ;
#2807=DIRECTION ( 'NONE',  ( 1.000000000000000000, 0.000000000000000000, 0.000000000000000000 ) ) ;
#2847=ORIENTED_EDGE ( 'NONE', *, *, #80, .T. ) ;
#2867=ORIENTED_EDGE ( 'NONE', *, *, #2190, .F. ) ;
#2904=DIRECTION ( 'NONE',  ( -0.000000000000000000, -0.000000000000000000, -1.000000000000000000 ) ) ;
#2907=EDGE_LOOP ( 'NONE', ( #733, #6025, #4196, #2154 ) ) ;
#2941=CLOSED_SHELL ( 'NONE', ( #3650, #7192, #226, #900, #7930, #6654, #4335, #4240, #827, #1873 ) ) ;
#2957=CARTESIAN_POINT ( 'NONE',  ( -0.04782642554762441683, -0.03125000000000000000, 0.07449999999999999678 ) ) ;
#2978=CARTESIAN_POINT ( 'NONE',  ( 0.2386870781737283065, -0.03125000000000000000, 0.07449999999999999678 ) ) ;
#3009=CARTESIAN_POINT ( 'NONE',  ( 0.6645694204159616758, 0.008319420416198241783, 0.07449999999999999678 ) ) ;
#3027=EDGE_CURVE ( 'NONE', #4512, #1200, #6470, .T. ) ;
#3086=( NAMED_UNIT ( * ) SI_UNIT ( $, .STERADIAN. ) SOLID_ANGLE_UNIT ( ) );
#3108=DIRECTION ( 'NONE',  ( -1.000000000000000000, 0.000000000000000000, 0.000000000000000000 ) ) ;
#3125=CARTESIAN_POINT ( 'NONE',  ( 0.2386870781737283065, -0.03125000000000000000, 0.07449999999999999678 ) ) ;
#3131=DIRECTION ( 'NONE',  ( -1.000000000000000000, -0.000000000000000000, -0.000000000000000000 ) ) ;
#3140=DIRECTION ( 'NONE',  ( 0.000000000000000000, 0.000000000000000000, 1.000000000000000000 ) ) ;
#3148=EDGE_CURVE ( 'NONE', #6628, #5472, #4173, .T. ) ;
#3195=ORIENTED_EDGE ( 'NONE', *, *, #5339, .F. ) ;
#3196=CARTESIAN_POINT ( 'NONE',  ( 0.7510138408322231118, -0.03124999999962550443, 0.07449999999999999678 ) ) ;
#3208=LINE ( 'NONE', #1312, #7896 ) ;
#3229=LINE ( 'NONE', #147, #5854 ) ;
#3258=LINE ( 'NONE', #4455, #5825 ) ;
#3286=PRODUCT ( 'Cleco, Fastener, Pincher', 'Cleco, Fastener, Pincher', '', ( #2796 ) ) ;
#3340=DIRECTION ( 'NONE',  ( 1.000000000000000000, 0.000000000000000000, 0.000000000000000000 ) ) ;
#3348=ORIENTED_EDGE ( 'NONE', *, *, #6423, .F. ) ;
#3372=AXIS2_PLACEMENT_3D ( 'NONE', #3636, #1822, #1700 ) ;
#3396=ORIENTED_EDGE ( 'NONE', *, *, #994, .F. ) ;
#3425=VERTEX_POINT ( 'NONE', #3705 ) ;
#3465=ORIENTED_EDGE ( 'NONE', *, *, #7536, .T. ) ;
#3474=APPLICATION_CONTEXT ( 'configuration controlled 3d designs of mechanical parts and assemblies' ) ;
#3488=EDGE_CURVE ( 'NONE', #6170, #4537, #6084, .T. ) ;
#3494=VECTOR ( 'NONE', #663, 39.37007874015748143 ) ;
#3536=EDGE_CURVE ( 'NONE', #1501, #4570, #167, .T. ) ;
#3555=AXIS2_PLACEMENT_3D ( 'NONE', #5720, #6981, #135 ) ;
#3593=MANIFOLD_SOLID_BREP ( 'Boss-Extrude1', #2941 ) ;
#3616=EDGE_LOOP ( 'NONE', ( #5007, #841, #6092, #1002, #3775, #1447, #1041, #1728 ) ) ;
#3627=( CONVERSION_BASED_UNIT ( 'INCH', #4970 ) LENGTH_UNIT ( ) NAMED_UNIT ( #6210 ) );
#3636=CARTESIAN_POINT ( 'NONE',  ( 0.6645694204159616758, 0.008319420416198241783, 0.07449999999999999678 ) ) ;
#3650=ADVANCED_FACE ( 'NONE', ( #2590 ), #5120, .F. ) ;
#3653=ORIENTED_EDGE ( 'NONE', *, *, #6091, .F. ) ;
#3665=( LENGTH_UNIT ( ) NAMED_UNIT ( * ) SI_UNIT ( $, .METRE. ) );
#3671=ORIENTED_EDGE ( 'NONE', *, *, #3685, .T. ) ;
#3682=ORIENTED_EDGE ( 'NONE', *, *, #6952, .F. ) ;
#3685=EDGE_CURVE ( 'NONE', #4537, #1200, #3208, .T. ) ;
#3699=EDGE_LOOP ( 'NONE', ( #4507, #5661, #3396, #959 ) ) ;
#3700=CARTESIAN_POINT ( 'NONE',  ( 0.6250000000000000000, -0.07812500000000001388, 0.07449999999999999678 ) ) ;
#3705=CARTESIAN_POINT ( 'NONE',  ( 0.2386870781737283065, -0.03125000000000000000, 0.000000000000000000 ) ) ;
#3775=ORIENTED_EDGE ( 'NONE', *, *, #3488, .T. ) ;
#3784=LINE ( 'NONE', #6128, #1791 ) ;
#3822=DIRECTION ( 'NONE',  ( -0.000000000000000000, -0.000000000000000000, -1.000000000000000000 ) ) ;
#3838=VECTOR ( 'NONE', #4384, 39.37007874015748143 ) ;
#3860=VECTOR ( 'NONE', #1433, 39.37007874015748143 ) ;
#3914=DIRECTION ( 'NONE',  ( -0.000000000000000000, -0.000000000000000000, -1.000000000000000000 ) ) ;
#3917=ORIENTED_EDGE ( 'NONE', *, *, #6499, .F. ) ;
#3937=DIRECTION ( 'NONE',  ( 0.000000000000000000, -1.000000000000000000, 0.000000000000000000 ) ) ;
#3950=DIRECTION ( 'NONE',  ( -1.000000000000000000, 0.000000000000000000, 0.000000000000000000 ) ) ;
#3951=DIRECTION ( 'NONE',  ( 1.000000000000000000, -1.821231995776175479E-16, 0.000000000000000000 ) ) ;
#3998=ORIENTED_EDGE ( 'NONE', *, *, #2780, .T. ) ;
#4010=ORIENTED_EDGE ( 'NONE', *, *, #2780, .F. ) ;
#4017=LINE ( 'NONE', #2732, #7022 ) ;
#4042=EDGE_CURVE ( 'NONE', #6252, #777, #4647, .T. ) ;
#4047=ORIENTED_EDGE ( 'NONE', *, *, #3536, .F. ) ;
#4083=PRODUCT_DEFINITION_FORMATION_WITH_SPECIFIED_SOURCE ( 'ANY', '', #3286, .NOT_KNOWN. ) ;
#4110=AXIS2_PLACEMENT_3D ( 'NONE', #910, #1625, #2735 ) ;
#4134=CARTESIAN_POINT ( 'NONE',  ( 0.6250000000000000000, -0.07812500000000001388, 0.07449999999999999678 ) ) ;
#4173=LINE ( 'NONE', #7968, #5290 ) ;
#4183=EDGE_CURVE ( 'NONE', #777, #1018, #2660, .T. ) ;
#4196=ORIENTED_EDGE ( 'NONE', *, *, #4183, .F. ) ;
#4213=DIRECTION ( 'NONE',  ( -1.000000000000000000, 0.000000000000000000, 0.000000000000000000 ) ) ;
#4219=ORIENTED_EDGE ( 'NONE', *, *, #4545, .F. ) ;
#4228=CARTESIAN_POINT ( 'NONE',  ( 0.2935750530104211387, 0.05119392622207447063, 0.07449999999999999678 ) ) ;
#4240=ADVANCED_FACE ( 'NONE', ( #2137 ), #6565, .F. ) ;
#4269=FACE_OUTER_BOUND ( 'NONE', #4321, .T. ) ;
#4321=EDGE_LOOP ( 'NONE', ( #922, #4219, #5611, #256 ) ) ;
#4335=ADVANCED_FACE ( 'NONE', ( #4269 ), #2252, .F. ) ;
#4384=DIRECTION ( 'NONE',  ( -1.000000000000000000, 0.000000000000000000, 0.000000000000000000 ) ) ;
#4455=CARTESIAN_POINT ( 'NONE',  ( -0.04782642554762442377, -0.07812500000000000000, 0.07449999999999999678 ) ) ;
#4458=ORIENTED_EDGE ( 'NONE', *, *, #330, .F. ) ;
#4464=LINE ( 'NONE', #1841, #5962 ) ;
#4478=AXIS2_PLACEMENT_3D ( 'NONE', #7099, #5612, #3108 ) ;
#4497=DIRECTION ( 'NONE',  ( -1.000000000000000000, 0.000000000000000000, 0.000000000000000000 ) ) ;
#4507=ORIENTED_EDGE ( 'NONE', *, *, #7489, .T. ) ;
#4512=VERTEX_POINT ( 'NONE', #14 ) ;
#4513=AXIS2_PLACEMENT_3D ( 'NONE', #7961, #6745, #5555 ) ;
#4529=ORIENTED_EDGE ( 'NONE', *, *, #7536, .F. ) ;
#4537=VERTEX_POINT ( 'NONE', #3196 ) ;
#4545=EDGE_CURVE ( 'NONE', #777, #1501, #4464, .T. ) ;
#4570=VERTEX_POINT ( 'NONE', #7576 ) ;
#4597=DIRECTION ( 'NONE',  ( -0.000000000000000000, 0.000000000000000000, -1.000000000000000000 ) ) ;
#4647=CIRCLE ( 'NONE', #4513, 0.03124999999999997571 ) ;
#4700=ORIENTED_EDGE ( 'NONE', *, *, #7489, .F. ) ;
#4728=APPLICATION_CONTEXT ( 'configuration controlled 3d designs of mechanical parts and assemblies' ) ;
#4835=CARTESIAN_POINT ( 'NONE',  ( 0.6690408158126811555, -0.04637372973215107830, 0.07449999999999999678 ) ) ;
#4902=ORIENTED_EDGE ( 'NONE', *, *, #80, .F. ) ;
#4905=FACE_OUTER_BOUND ( 'NONE', #5654, .T. ) ;
#4925=DIRECTION ( 'NONE',  ( 0.000000000000000000, -1.000000000000000000, 0.000000000000000000 ) ) ;
#4965=ORIENTED_EDGE ( 'NONE', *, *, #3027, .F. ) ;
#4970=LENGTH_MEASURE_WITH_UNIT ( LENGTH_MEASURE( 0.02539999999999999897 ), #3665 );
#5007=ORIENTED_EDGE ( 'NONE', *, *, #6952, .T. ) ;
#5009=DIRECTION ( 'NONE',  ( -0.000000000000000000, -0.000000000000000000, -1.000000000000000000 ) ) ;
#5024=SHAPE_REPRESENTATION ( 'Cleco, Fastener, Pincher', ( #3555 ), #553 ) ;
#5075=DIRECTION ( 'NONE',  ( 0.000000000000000000, 0.000000000000000000, 1.000000000000000000 ) ) ;
#5079=DIRECTION ( 'NONE',  ( -0.000000000000000000, -0.000000000000000000, -1.000000000000000000 ) ) ;
#5090=CARTESIAN_POINT ( 'NONE',  ( 0.2896281645421511231, -0.04777128394798136474, 0.000000000000000000 ) ) ;
#5093=EDGE_CURVE ( 'NONE', #4537, #6252, #48, .T. ) ;
#5120=CYLINDRICAL_SURFACE ( 'NONE', #711, 0.09904388296398869418 ) ;
#5171=DIRECTION ( 'NONE',  ( -0.000000000000000000, -0.000000000000000000, -1.000000000000000000 ) ) ;
#5196=AXIS2_PLACEMENT_3D ( 'NONE', #8084, #432, #6177 ) ;
#5290=VECTOR ( 'NONE', #4213, 39.37007874015748143 ) ;
#5311=VECTOR ( 'NONE', #6018, 39.37007874015748143 ) ;
#5339=EDGE_CURVE ( 'NONE', #7690, #1501, #7174, .T. ) ;
#5460=CIRCLE ( 'NONE', #7810, 0.3547681700190749576 ) ;
#5461=FACE_OUTER_BOUND ( 'NONE', #7352, .T. ) ;
#5472=VERTEX_POINT ( 'NONE', #2307 ) ;
#5487=EDGE_CURVE ( 'NONE', #5976, #6170, #6658, .T. ) ;
#5506=DIRECTION ( 'NONE',  ( 0.000000000000000000, 0.000000000000000000, 1.000000000000000000 ) ) ;
#5513=CARTESIAN_POINT ( 'NONE',  ( 0.7739487307887357170, -0.3852760516983189110, 0.07449999999999999678 ) ) ;
#5555=DIRECTION ( 'NONE',  ( 1.000000000000000000, 0.000000000000000000, 0.000000000000000000 ) ) ;
#5585=LINE ( 'NONE', #3700, #5933 ) ;
#5611=ORIENTED_EDGE ( 'NONE', *, *, #4042, .F. ) ;
#5612=DIRECTION ( 'NONE',  ( -0.000000000000000000, 0.000000000000000000, -1.000000000000000000 ) ) ;
#5618=ORIENTED_EDGE ( 'NONE', *, *, #3685, .F. ) ;
#5654=EDGE_LOOP ( 'NONE', ( #2071, #4458, #459, #3671 ) ) ;
#5661=ORIENTED_EDGE ( 'NONE', *, *, #270, .F. ) ;
#5682=PLANE ( 'NONE',  #1634 ) ;
#5684=AXIS2_PLACEMENT_3D ( 'NONE', #3009, #5506, #7991 ) ;
#5720=CARTESIAN_POINT ( 'NONE',  ( 0.000000000000000000, 0.000000000000000000, 0.000000000000000000 ) ) ;
#5753=PLANE ( 'NONE',  #4478 ) ;
#5760=CARTESIAN_POINT ( 'NONE',  ( -0.04782642554762441683, -0.03125000000000000000, 0.000000000000000000 ) ) ;
#5824=CARTESIAN_POINT ( 'NONE',  ( 0.6690408158126811555, -0.04637372973215107830, 0.000000000000000000 ) ) ;
#5825=VECTOR ( 'NONE', #7721, 39.37007874015748143 ) ;
#5846=CIRCLE ( 'NONE', #2303, 0.09904388296398869418 ) ;
#5854=VECTOR ( 'NONE', #2641, 39.37007874015748143 ) ;
#5905=DIRECTION ( 'NONE',  ( -1.000000000000000000, 0.000000000000000000, 0.000000000000000000 ) ) ;
#5933=VECTOR ( 'NONE', #1769, 39.37007874015748143 ) ;
#5957=AXIS2_PLACEMENT_3D ( 'NONE', #1031, #2904, #6766 ) ;
#5962=VECTOR ( 'NONE', #5079, 39.37007874015748143 ) ;
#5976=VERTEX_POINT ( 'NONE', #6475 ) ;
#6001=PRODUCT_DEFINITION ( 'UNKNOWN', '', #4083, #2765 ) ;
#6018=DIRECTION ( 'NONE',  ( 1.000000000000000000, 0.000000000000000000, 0.000000000000000000 ) ) ;
#6025=ORIENTED_EDGE ( 'NONE', *, *, #6442, .F. ) ;
#6084=CIRCLE ( 'NONE', #5684, 0.09507037842118626347 ) ;
#6091=EDGE_CURVE ( 'NONE', #4570, #3425, #5846, .T. ) ;
#6092=ORIENTED_EDGE ( 'NONE', *, *, #994, .T. ) ;
#6111=CARTESIAN_POINT ( 'NONE',  ( 0.6597999294535048520, -0.04777128394798136474, 0.000000000000000000 ) ) ;
#6122=FACE_OUTER_BOUND ( 'NONE', #7684, .T. ) ;
#6128=CARTESIAN_POINT ( 'NONE',  ( 0.2386870781737283065, -0.03125000000000000000, 0.07449999999999999678 ) ) ;
#6170=VERTEX_POINT ( 'NONE', #4134 ) ;
#6177=DIRECTION ( 'NONE',  ( -1.000000000000000000, 0.000000000000000000, 0.000000000000000000 ) ) ;
#6210=DIMENSIONAL_EXPONENTS ( 1.000000000000000000, 0.000000000000000000, 0.000000000000000000, 0.000000000000000000, 0.000000000000000000, 0.000000000000000000, 0.000000000000000000 ) ;
#6244=CARTESIAN_POINT ( 'NONE',  ( -0.04782642554762442377, -0.07812500000000000000, 0.07449999999999999678 ) ) ;
#6252=VERTEX_POINT ( 'NONE', #4835 ) ;
#6302=CARTESIAN_POINT ( 'NONE',  ( -0.04782642554762441683, -0.03125000000000000000, 0.07449999999999999678 ) ) ;
#6403=CARTESIAN_POINT ( 'NONE',  ( 0.2935750530104211387, 0.05119392622207447063, 0.07449999999999999678 ) ) ;
#6423=EDGE_CURVE ( 'NONE', #1200, #7690, #5460, .T. ) ;
#6442=EDGE_CURVE ( 'NONE', #1018, #4570, #3229, .T. ) ;
#6470=CIRCLE ( 'NONE', #4110, 0.09507037842118626347 ) ;
#6475=CARTESIAN_POINT ( 'NONE',  ( -0.04782642554762442377, -0.07812500000000000000, 0.07449999999999999678 ) ) ;
#6499=EDGE_CURVE ( 'NONE', #5472, #6917, #4017, .T. ) ;
#6521=DIRECTION ( 'NONE',  ( -0.000000000000000000, -0.000000000000000000, -1.000000000000000000 ) ) ;
#6565=PLANE ( 'NONE',  #582 ) ;
#6627=LINE ( 'NONE', #2048, #5311 ) ;
#6628=VERTEX_POINT ( 'NONE', #2978 ) ;
#6654=ADVANCED_FACE ( 'NONE', ( #4905 ), #2352, .T. ) ;
#6658=LINE ( 'NONE', #381, #2713 ) ;
#6745=DIRECTION ( 'NONE',  ( -0.000000000000000000, -0.000000000000000000, -1.000000000000000000 ) ) ;
#6746=FACE_OUTER_BOUND ( 'NONE', #608, .T. ) ;
#6766=DIRECTION ( 'NONE',  ( -1.000000000000000000, 0.000000000000000000, 0.000000000000000000 ) ) ;
#6868=CARTESIAN_POINT ( 'NONE',  ( -0.04782642554762442377, -0.07812500000000000000, 0.000000000000000000 ) ) ;
#6917=VERTEX_POINT ( 'NONE', #5760 ) ;
#6929=DIRECTION ( 'NONE',  ( 0.000000000000000000, -0.000000000000000000, -1.000000000000000000 ) ) ;
#6952=EDGE_CURVE ( 'NONE', #1018, #6628, #7685, .T. ) ;
#6981=DIRECTION ( 'NONE',  ( 0.000000000000000000, 0.000000000000000000, 1.000000000000000000 ) ) ;
#7022=VECTOR ( 'NONE', #6521, 39.37007874015748143 ) ;
#7099=CARTESIAN_POINT ( 'NONE',  ( 0.2935750530104211387, 0.05119392622207447063, 0.000000000000000000 ) ) ;
#7174=CIRCLE ( 'NONE', #7693, 0.03124999999999997571 ) ;
#7185=DIRECTION ( 'NONE',  ( -1.000000000000000000, 0.000000000000000000, 0.000000000000000000 ) ) ;
#7192=ADVANCED_FACE ( 'NONE', ( #6122 ), #7502, .F. ) ;
#7291=CARTESIAN_POINT ( 'NONE',  ( 0.2935750530104211387, 0.05119392622207447063, 0.000000000000000000 ) ) ;
#7352=EDGE_LOOP ( 'NONE', ( #2847, #2867, #1839, #7952 ) ) ;
#7380=DIRECTION ( 'NONE',  ( 0.000000000000000000, 1.000000000000000000, 0.000000000000000000 ) ) ;
#7384=VECTOR ( 'NONE', #3131, 39.37007874015748143 ) ;
#7422=SHAPE_DEFINITION_REPRESENTATION ( #2109, #5024 ) ;
#7489=EDGE_CURVE ( 'NONE', #6917, #1875, #7, .T. ) ;
#7502=PLANE ( 'NONE',  #8067 ) ;
#7536=EDGE_CURVE ( 'NONE', #6628, #3425, #3784, .T. ) ;
#7542=ORIENTED_EDGE ( 'NONE', *, *, #6091, .T. ) ;
#7566=LINE ( 'NONE', #1492, #2683 ) ;
#7567=ORIENTED_EDGE ( 'NONE', *, *, #3488, .F. ) ;
#7576=CARTESIAN_POINT ( 'NONE',  ( 0.2896281645421511231, -0.04777128394798136474, 0.000000000000000000 ) ) ;
#7668=SHAPE_REPRESENTATION_RELATIONSHIP ( 'NONE' , 'NONE' ,  #5024, #1981 ) ;
#7684=EDGE_LOOP ( 'NONE', ( #3998, #3917, #2636, #3465 ) ) ;
#7685=CIRCLE ( 'NONE', #2315, 0.09904388296398869418 ) ;
#7690=VERTEX_POINT ( 'NONE', #5824 ) ;
#7693=AXIS2_PLACEMENT_3D ( 'NONE', #2020, #1361, #3340 ) ;
#7720=DIRECTION ( 'NONE',  ( -0.000000000000000000, -0.000000000000000000, -1.000000000000000000 ) ) ;
#7721=DIRECTION ( 'NONE',  ( -0.000000000000000000, -0.000000000000000000, -1.000000000000000000 ) ) ;
#7752=FACE_OUTER_BOUND ( 'NONE', #3616, .T. ) ;
#7810=AXIS2_PLACEMENT_3D ( 'NONE', #2567, #5075, #4497 ) ;
#7896=VECTOR ( 'NONE', #3822, 39.37007874015748143 ) ;
#7930=ADVANCED_FACE ( 'NONE', ( #6746 ), #2314, .T. ) ;
#7949=PLANE ( 'NONE',  #2425 ) ;
#7952=ORIENTED_EDGE ( 'NONE', *, *, #270, .T. ) ;
#7961=CARTESIAN_POINT ( 'NONE',  ( 0.6597999294535048520, -0.01652128394798136821, 0.07449999999999999678 ) ) ;
#7968=CARTESIAN_POINT ( 'NONE',  ( 0.2386870781737283065, -0.03125000000000000000, 0.07449999999999999678 ) ) ;
#7991=DIRECTION ( 'NONE',  ( 1.000000000000000000, 0.000000000000000000, 0.000000000000000000 ) ) ;
#8067=AXIS2_PLACEMENT_3D ( 'NONE', #3125, #4925, #6929 ) ;
#8071=CARTESIAN_POINT ( 'NONE',  ( -0.04782642554762441683, -0.03125000000000000000, 0.000000000000000000 ) ) ;
#8084=CARTESIAN_POINT ( 'NONE',  ( 0.7739487307887357170, -0.3852760516983189110, 0.07449999999999999678 ) ) ;
#8115=COLOUR_RGB('Sky Blue', 0.40784314, 0.44705882, 0.49803922);
#8116=FILL_AREA_STYLE_COLOUR('',#8115);
#8117=FILL_AREA_STYLE('',(#8116));
#8118=SURFACE_STYLE_FILL_AREA(#8117);
#8119=SURFACE_SIDE_STYLE('',(#8118));
#8120=SURFACE_STYLE_USAGE(.BOTH.,#8119);
#8121=PRESENTATION_STYLE_ASSIGNMENT((#8120));
#8143=STYLED_ITEM('',(#8121),#3593);
#8144=MECHANICAL_DESIGN_GEOMETRIC_PRESENTATION_REPRESENTATION('',(#8143),#553);
ENDSEC;
END-ISO-10303-21;
